ISO-10303-21;
HEADER;
/* Generated by software containing ST-Developer
 * from STEP Tools, Inc. (www.steptools.com) 
 */

FILE_DESCRIPTION(
/* description */ ('Turntable on roller ring'),
/* implementation_level */ '2;1');

FILE_NAME(
/* name */ 'Roller axle (2).step',
/* time_stamp */ '2026-10-28T03:23:59-07:00',
/* author */ (''),
/* organization */ (''),
/* preprocessor_version */ 'ST-DEVELOPER v20.2',
/* originating_system */ 'Autodesk Translation Framework v15.17.0.0',
/* authorisation */ '');

FILE_SCHEMA (('AUTOMOTIVE_DESIGN { 1 0 10303 214 3 1 1 }'));
ENDSEC;

DATA;
#10=MECHANICAL_DESIGN_GEOMETRIC_PRESENTATION_REPRESENTATION('',(#653),#16281);
#534=SHAPE_REPRESENTATION_RELATIONSHIP('SRR','None',#16553,#589);
#589=ADVANCED_BREP_SHAPE_REPRESENTATION('',(#723),#16247);
#653=STYLED_ITEM('',(#16932),#723);
#723=MANIFOLD_SOLID_BREP('Body1',#8396);
#925=FACE_BOUND('',#2240,.T.);
#926=FACE_BOUND('',#2245,.T.);
#1151=PLANE('',#9726);
#1152=PLANE('',#9727);
#1153=PLANE('',#9732);
#1154=PLANE('',#9735);
#1564=FACE_OUTER_BOUND('',#2237,.T.);
#1565=FACE_OUTER_BOUND('',#2238,.T.);
#1566=FACE_OUTER_BOUND('',#2239,.T.);
#1567=FACE_OUTER_BOUND('',#2241,.T.);
#1568=FACE_OUTER_BOUND('',#2242,.T.);
#1569=FACE_OUTER_BOUND('',#2243,.T.);
#1570=FACE_OUTER_BOUND('',#2244,.T.);
#2237=EDGE_LOOP('',(#6977,#6978,#6979,#6980));
#2238=EDGE_LOOP('',(#6981));
#2239=EDGE_LOOP('',(#6982));
#2240=EDGE_LOOP('',(#6983));
#2241=EDGE_LOOP('',(#6984,#6985,#6986,#6987));
#2242=EDGE_LOOP('',(#6988));
#2243=EDGE_LOOP('',(#6989,#6990,#6991,#6992));
#2244=EDGE_LOOP('',(#6993));
#2245=EDGE_LOOP('',(#6994));
#2830=LINE('',#14931,#3313);
#2831=LINE('',#14941,#3314);
#2832=LINE('',#14947,#3315);
#3313=VECTOR('',#11907,0.165);
#3314=VECTOR('',#11920,0.8);
#3315=VECTOR('',#11929,0.5);
#3767=CIRCLE('',#9724,0.165);
#3768=CIRCLE('',#9725,0.165);
#3769=CIRCLE('',#9728,0.8);
#3770=CIRCLE('',#9729,0.5);
#3771=CIRCLE('',#9731,0.8);
#3772=CIRCLE('',#9734,0.5);
#4395=VERTEX_POINT('',#14928);
#4396=VERTEX_POINT('',#14930);
#4397=VERTEX_POINT('',#14935);
#4398=VERTEX_POINT('',#14937);
#4399=VERTEX_POINT('',#14940);
#4400=VERTEX_POINT('',#14945);
#5299=EDGE_CURVE('',#4395,#4395,#3767,.T.);
#5300=EDGE_CURVE('',#4395,#4396,#2830,.T.);
#5301=EDGE_CURVE('',#4396,#4396,#3768,.T.);
#5302=EDGE_CURVE('',#4397,#4397,#3769,.T.);
#5303=EDGE_CURVE('',#4398,#4398,#3770,.T.);
#5304=EDGE_CURVE('',#4397,#4399,#2831,.T.);
#5305=EDGE_CURVE('',#4399,#4399,#3771,.T.);
#5306=EDGE_CURVE('',#4400,#4400,#3772,.T.);
#5307=EDGE_CURVE('',#4400,#4398,#2832,.T.);
#6977=ORIENTED_EDGE('',*,*,#5299,.F.);
#6978=ORIENTED_EDGE('',*,*,#5300,.T.);
#6979=ORIENTED_EDGE('',*,*,#5301,.F.);
#6980=ORIENTED_EDGE('',*,*,#5300,.F.);
#6981=ORIENTED_EDGE('',*,*,#5299,.T.);
#6982=ORIENTED_EDGE('',*,*,#5302,.T.);
#6983=ORIENTED_EDGE('',*,*,#5303,.F.);
#6984=ORIENTED_EDGE('',*,*,#5302,.F.);
#6985=ORIENTED_EDGE('',*,*,#5304,.T.);
#6986=ORIENTED_EDGE('',*,*,#5305,.T.);
#6987=ORIENTED_EDGE('',*,*,#5304,.F.);
#6988=ORIENTED_EDGE('',*,*,#5305,.F.);
#6989=ORIENTED_EDGE('',*,*,#5306,.F.);
#6990=ORIENTED_EDGE('',*,*,#5307,.T.);
#6991=ORIENTED_EDGE('',*,*,#5303,.T.);
#6992=ORIENTED_EDGE('',*,*,#5307,.F.);
#6993=ORIENTED_EDGE('',*,*,#5306,.T.);
#6994=ORIENTED_EDGE('',*,*,#5301,.T.);
#7789=CYLINDRICAL_SURFACE('',#9723,0.165);
#7790=CYLINDRICAL_SURFACE('',#9730,0.8);
#7791=CYLINDRICAL_SURFACE('',#9733,0.5);
#8167=ADVANCED_FACE('',(#1564),#7789,.F.);
#8168=ADVANCED_FACE('',(#1565),#1151,.T.);
#8169=ADVANCED_FACE('',(#1566,#925),#1152,.T.);
#8170=ADVANCED_FACE('',(#1567),#7790,.T.);
#8171=ADVANCED_FACE('',(#1568),#1153,.F.);
#8172=ADVANCED_FACE('',(#1569),#7791,.T.);
#8173=ADVANCED_FACE('',(#1570,#926),#1154,.T.);
#8396=CLOSED_SHELL('',(#8167,#8168,#8169,#8170,#8171,#8172,#8173));
#9722=AXIS2_PLACEMENT_3D('',#14926,#11901,#11902);
#9723=AXIS2_PLACEMENT_3D('',#14927,#11903,#11904);
#9724=AXIS2_PLACEMENT_3D('',#14929,#11905,#11906);
#9725=AXIS2_PLACEMENT_3D('',#14932,#11908,#11909);
#9726=AXIS2_PLACEMENT_3D('',#14933,#11910,#11911);
#9727=AXIS2_PLACEMENT_3D('',#14934,#11912,#11913);
#9728=AXIS2_PLACEMENT_3D('',#14936,#11914,#11915);
#9729=AXIS2_PLACEMENT_3D('',#14938,#11916,#11917);
#9730=AXIS2_PLACEMENT_3D('',#14939,#11918,#11919);
#9731=AXIS2_PLACEMENT_3D('',#14942,#11921,#11922);
#9732=AXIS2_PLACEMENT_3D('',#14943,#11923,#11924);
#9733=AXIS2_PLACEMENT_3D('',#14944,#11925,#11926);
#9734=AXIS2_PLACEMENT_3D('',#14946,#11927,#11928);
#9735=AXIS2_PLACEMENT_3D('',#14948,#11930,#11931);
#11901=DIRECTION('axis',(0.,0.,1.));
#11902=DIRECTION('refdir',(1.,0.,0.));
#11903=DIRECTION('center_axis',(0.,1.,0.));
#11904=DIRECTION('ref_axis',(1.,0.,0.));
#11905=DIRECTION('center_axis',(0.,1.,0.));
#11906=DIRECTION('ref_axis',(1.,0.,0.));
#11907=DIRECTION('',(0.,1.,0.));
#11908=DIRECTION('center_axis',(0.,-1.,0.));
#11909=DIRECTION('ref_axis',(1.,0.,0.));
#11910=DIRECTION('center_axis',(0.,1.,0.));
#11911=DIRECTION('ref_axis',(1.,0.,0.));
#11912=DIRECTION('center_axis',(0.,1.,0.));
#11913=DIRECTION('ref_axis',(1.,0.,0.));
#11914=DIRECTION('center_axis',(0.,1.,0.));
#11915=DIRECTION('ref_axis',(1.,0.,0.));
#11916=DIRECTION('center_axis',(0.,1.,0.));
#11917=DIRECTION('ref_axis',(1.,0.,0.));
#11918=DIRECTION('center_axis',(0.,1.,0.));
#11919=DIRECTION('ref_axis',(1.,0.,0.));
#11920=DIRECTION('',(0.,-1.,0.));
#11921=DIRECTION('center_axis',(0.,1.,0.));
#11922=DIRECTION('ref_axis',(1.,0.,0.));
#11923=DIRECTION('center_axis',(0.,1.,0.));
#11924=DIRECTION('ref_axis',(1.,0.,0.));
#11925=DIRECTION('center_axis',(0.,1.,0.));
#11926=DIRECTION('ref_axis',(1.,0.,0.));
#11927=DIRECTION('center_axis',(0.,1.,0.));
#11928=DIRECTION('ref_axis',(1.,0.,0.));
#11929=DIRECTION('',(0.,-1.,0.));
#11930=DIRECTION('center_axis',(0.,1.,0.));
#11931=DIRECTION('ref_axis',(1.,0.,0.));
#14926=CARTESIAN_POINT('',(0.,0.,0.));
#14927=CARTESIAN_POINT('Origin',(0.,15.2,3.5));
#14928=CARTESIAN_POINT('',(-0.165,15.2,3.5));
#14929=CARTESIAN_POINT('Origin',(0.,15.2,3.5));
#14930=CARTESIAN_POINT('',(-0.165,16.3,3.5));
#14931=CARTESIAN_POINT('',(-0.165,15.2,3.5));
#14932=CARTESIAN_POINT('Origin',(0.,16.3,3.5));
#14933=CARTESIAN_POINT('Origin',(0.,15.2,3.5));
#14934=CARTESIAN_POINT('Origin',(0.,13.7,3.5));
#14935=CARTESIAN_POINT('',(-0.8,13.7,3.5));
#14936=CARTESIAN_POINT('Origin',(0.,13.7,3.5));
#14937=CARTESIAN_POINT('',(-0.5,13.7,3.5));
#14938=CARTESIAN_POINT('Origin',(0.,13.7,3.5));
#14939=CARTESIAN_POINT('Origin',(0.,13.3,3.5));
#14940=CARTESIAN_POINT('',(-0.8,13.3,3.5));
#14941=CARTESIAN_POINT('',(-0.8,13.3,3.5));
#14942=CARTESIAN_POINT('Origin',(0.,13.3,3.5));
#14943=CARTESIAN_POINT('Origin',(0.,13.3,3.5));
#14944=CARTESIAN_POINT('Origin',(0.,13.7,3.5));
#14945=CARTESIAN_POINT('',(-0.5,16.3,3.5));
#14946=CARTESIAN_POINT('Origin',(0.,16.3,3.5));
#14947=CARTESIAN_POINT('',(-0.5,13.7,3.5));
#14948=CARTESIAN_POINT('Origin',(0.,16.3,3.5));
#16178=UNCERTAINTY_MEASURE_WITH_UNIT(LENGTH_MEASURE(0.001),#16282,
'DISTANCE_ACCURACY_VALUE',
'Maximum model space distance between geometric entities at asserted c
onnectivities');
#16212=UNCERTAINTY_MEASURE_WITH_UNIT(LENGTH_MEASURE(0.001),#16282,
'DISTANCE_ACCURACY_VALUE',
'Maximum model space distance between geometric entities at asserted c
onnectivities');
#16247=(
GEOMETRIC_REPRESENTATION_CONTEXT(3)
GLOBAL_UNCERTAINTY_ASSIGNED_CONTEXT((#16178))
GLOBAL_UNIT_ASSIGNED_CONTEXT((#16282,#16284,#16285))
REPRESENTATION_CONTEXT('','3D')
);
#16281=(
GEOMETRIC_REPRESENTATION_CONTEXT(3)
GLOBAL_UNCERTAINTY_ASSIGNED_CONTEXT((#16212))
GLOBAL_UNIT_ASSIGNED_CONTEXT((#16282,#16284,#16285))
REPRESENTATION_CONTEXT('','3D')
);
#16282=(
LENGTH_UNIT()
NAMED_UNIT(*)
SI_UNIT(.CENTI.,.METRE.)
);
#16284=(
NAMED_UNIT(*)
PLANE_ANGLE_UNIT()
SI_UNIT($,.RADIAN.)
);
#16285=(
NAMED_UNIT(*)
SI_UNIT($,.STERADIAN.)
SOLID_ANGLE_UNIT()
);
#16320=SHAPE_DEFINITION_REPRESENTATION(#16414,#16553);
#16414=PRODUCT_DEFINITION_SHAPE('',$,#16622);
#16553=SHAPE_REPRESENTATION('',(#9722),#16247);
#16587=PRODUCT_DEFINITION_CONTEXT('part definition',#16793,'design');
#16622=PRODUCT_DEFINITION('Roller axle (2)','Roller axle (2)',#16690,#16587);
#16690=PRODUCT_DEFINITION_FORMATION('',$,#16829);
#16793=APPLICATION_CONTEXT(
'Core Data for Automotive Mechanical Design Process');
#16794=PRODUCT_CONTEXT('part definition',#16793,'mechanical');
#16829=PRODUCT('Roller axle (2)','Roller axle (2)','Roller axle (2)',(#16794));
#16926=COLOUR_RGB('Grey',0.48,0.52,0.57);
#16927=FILL_AREA_STYLE_COLOUR('',#16926);
#16928=FILL_AREA_STYLE('',(#16927));
#16929=SURFACE_STYLE_FILL_AREA(#16928);
#16930=SURFACE_SIDE_STYLE('',(#16929));
#16931=SURFACE_STYLE_USAGE(.BOTH.,#16930);
#16932=PRESENTATION_STYLE_ASSIGNMENT((#16931));
ENDSEC;
END-ISO-10303-21;
